ISO-10303-21;
HEADER;
FILE_DESCRIPTION (('STEP AP214'),
    '1' );
FILE_NAME ('circlip for shafts heavy_din_Circlip DIN 471 - 60 x 3.step',
    '2026-10-23T05:12:30',
    ( '' ),
    ( '' ),
    'SwSTEP 2.0',
    'SolidWorks 2026',
    '' );
FILE_SCHEMA (( 'AUTOMOTIVE_DESIGN' ));
ENDSEC;

DATA;
#1=LINE ( 'NONE', #2495, #1142 ) ;
#11=CARTESIAN_POINT ( 'NONE',  ( 5.459126460941067016, -34.89491303563345070, -3.000000000000000000 ) ) ;
#12=CIRCLE ( 'NONE', #1262, 6.099504629071905271 ) ;
#30=ORIENTED_EDGE ( 'NONE', *, *, #1780, .F. ) ;
#32=EDGE_CURVE ( 'NONE', #3001, #1611, #576, .T. ) ;
#56=DIRECTION ( 'NONE',  ( 1.000000000000000000, 0.000000000000000000, 0.000000000000000000 ) ) ;
#58=VECTOR ( 'NONE', #4339, 1000.000000000000000 ) ;
#63=CARTESIAN_POINT ( 'NONE',  ( 1.499999999999999334, -33.63777638310832430, 0.000000000000000000 ) ) ;
#83=CYLINDRICAL_SURFACE ( 'NONE', #246, 6.099504629071905271 ) ;
#92=DIRECTION ( 'NONE',  ( 0.000000000000000000, 0.000000000000000000, 1.000000000000000000 ) ) ;
#93=CARTESIAN_POINT ( 'NONE',  ( 4.586480920263560357, -37.21846574978686562, -3.000000000000000000 ) ) ;
#100=DIRECTION ( 'NONE',  ( 1.000000000000000000, 0.000000000000000000, 0.000000000000000000 ) ) ;
#133=CARTESIAN_POINT ( 'NONE',  ( -32.81578194438969120, 1.484218055610309728, 0.000000000000000000 ) ) ;
#136=DIRECTION ( 'NONE',  ( 0.000000000000000000, 0.000000000000000000, 1.000000000000000000 ) ) ;
#137=LINE ( 'NONE', #2482, #1537 ) ;
#148=EDGE_LOOP ( 'NONE', ( #2715, #5380, #1534, #3342 ) ) ;
#151=CARTESIAN_POINT ( 'NONE',  ( -5.459126460941067016, -34.89491303563345070, 0.000000000000000000 ) ) ;
#156=ORIENTED_EDGE ( 'NONE', *, *, #2886, .T. ) ;
#163=DIRECTION ( 'NONE',  ( 1.000000000000000000, 0.000000000000000000, 0.000000000000000000 ) ) ;
#169=DIRECTION ( 'NONE',  ( 1.000000000000000000, 0.000000000000000000, 0.000000000000000000 ) ) ;
#196=CARTESIAN_POINT ( 'NONE',  ( -0.5700000000000001732, -28.49429942988597020, -3.000000000000000000 ) ) ;
#210=AXIS2_PLACEMENT_3D ( 'NONE', #7506, #2784, #5179 ) ;
#216=CARTESIAN_POINT ( 'NONE',  ( 4.000000000000000000, -33.63777638310832430, -3.000000000000000000 ) ) ;
#227=VECTOR ( 'NONE', #3090, 1000.000000000000000 ) ;
#234=VECTOR ( 'NONE', #92, 1000.000000000000000 ) ;
#237=ORIENTED_EDGE ( 'NONE', *, *, #4138, .F. ) ;
#242=CIRCLE ( 'NONE', #872, 0.7500000000000041078 ) ;
#244=EDGE_LOOP ( 'NONE', ( #4274, #4627, #3628, #1463, #5044, #4969, #332, #6418, #2566, #3083, #602, #296, #1781, #3453, #237, #2234 ) ) ;
#246=AXIS2_PLACEMENT_3D ( 'NONE', #7304, #4299, #6708 ) ;
#268=EDGE_CURVE ( 'NONE', #736, #6870, #4277, .T. ) ;
#278=ORIENTED_EDGE ( 'NONE', *, *, #4857, .T. ) ;
#296=ORIENTED_EDGE ( 'NONE', *, *, #5918, .F. ) ;
#308=DIRECTION ( 'NONE',  ( -0.000000000000000000, -0.000000000000000000, -1.000000000000000000 ) ) ;
#310=CARTESIAN_POINT ( 'NONE',  ( 5.459126460941064352, -34.89491303563345070, 0.000000000000000000 ) ) ;
#317=PLANE ( 'NONE',  #5373 ) ;
#328=DIRECTION ( 'NONE',  ( 0.000000000000000000, 0.000000000000000000, 1.000000000000000000 ) ) ;
#330=FACE_OUTER_BOUND ( 'NONE', #2807, .T. ) ;
#332=ORIENTED_EDGE ( 'NONE', *, *, #4857, .F. ) ;
#352=ORIENTED_EDGE ( 'NONE', *, *, #4240, .F. ) ;
#355=CYLINDRICAL_SURFACE ( 'NONE', #1081, 0.7500000000000041078 ) ;
#371=VERTEX_POINT ( 'NONE', #5060 ) ;
#386=CARTESIAN_POINT ( 'NONE',  ( 0.000000000000000000, 0.000000000000000000, 0.000000000000000000 ) ) ;
#393=ORIENTED_EDGE ( 'NONE', *, *, #5918, .T. ) ;
#417=DIRECTION ( 'NONE',  ( 0.000000000000000000, 0.000000000000000000, 1.000000000000000000 ) ) ;
#418=ORIENTED_EDGE ( 'NONE', *, *, #2868, .T. ) ;
#421=VERTEX_POINT ( 'NONE', #3959 ) ;
#434=FACE_OUTER_BOUND ( 'NONE', #851, .T. ) ;
#453=EDGE_CURVE ( 'NONE', #421, #4626, #6250, .T. ) ;
#454=DIRECTION ( 'NONE',  ( 0.1305261922200541547, -0.9914448613738101601, 0.000000000000000000 ) ) ;
#463=EDGE_CURVE ( 'NONE', #7599, #5285, #2102, .T. ) ;
#473=EDGE_LOOP ( 'NONE', ( #5151, #6491, #2990, #3433 ) ) ;
#475=MANIFOLD_SOLID_BREP ( 'Body', #5362 ) ;
#476=CIRCLE ( 'NONE', #4885, 6.099504629071904382 ) ;
#487=CARTESIAN_POINT ( 'NONE',  ( 0.000000000000000000, 1.484218055610305731, -3.000000000000000000 ) ) ;
#500=CYLINDRICAL_SURFACE ( 'NONE', #990, 28.49999999999999645 ) ;
#502=VERTEX_POINT ( 'NONE', #3884 ) ;
#505=LINE ( 'NONE', #547, #511 ) ;
#511=VECTOR ( 'NONE', #2920, 999.9999999999998863 ) ;
#517=CARTESIAN_POINT ( 'NONE',  ( 0.000000000000000000, 0.000000000000000000, -3.000000000000000000 ) ) ;
#527=CARTESIAN_POINT ( 'NONE',  ( 28.49999999999999645, 0.000000000000000000, -3.000000000000000000 ) ) ;
#528=CYLINDRICAL_SURFACE ( 'NONE', #6274, 1.250000000000000222 ) ;
#545=VERTEX_POINT ( 'NONE', #7662 ) ;
#546=AXIS2_PLACEMENT_3D ( 'NONE', #386, #1018, #2806 ) ;
#547=CARTESIAN_POINT ( 'NONE',  ( 5.459126460941067016, -34.89491303563345070, -3.000000000000000000 ) ) ;
#576=CIRCLE ( 'NONE', #3727, 1.250000000000000222 ) ;
#602=ORIENTED_EDGE ( 'NONE', *, *, #3937, .F. ) ;
#603=DIRECTION ( 'NONE',  ( 0.000000000000000000, 0.000000000000000000, 1.000000000000000000 ) ) ;
#610=EDGE_CURVE ( 'NONE', #7629, #6982, #1196, .T. ) ;
#611=CARTESIAN_POINT ( 'NONE',  ( -2.750000000000000000, -33.63777638310832430, 0.000000000000000000 ) ) ;
#615=CARTESIAN_POINT ( 'NONE',  ( -9.702951051037022268, -29.86427928513813512, -3.000000000000000000 ) ) ;
#623=DIRECTION ( 'NONE',  ( -0.9997999799959990108, -0.01999999999999999001, 0.000000000000000000 ) ) ;
#645=CARTESIAN_POINT ( 'NONE',  ( -5.459126460941067016, -34.89491303563345070, -3.000000000000000000 ) ) ;
#646=DIRECTION ( 'NONE',  ( -0.000000000000000000, -0.000000000000000000, -1.000000000000000000 ) ) ;
#647=LINE ( 'NONE', #93, #4504 ) ;
#648=DIRECTION ( 'NONE',  ( 0.000000000000000000, 0.000000000000000000, 1.000000000000000000 ) ) ;
#656=LINE ( 'NONE', #1850, #7180 ) ;
#674=DIRECTION ( 'NONE',  ( 0.1305261922200541547, -0.9914448613738101601, 0.000000000000000000 ) ) ;
#678=ORIENTED_EDGE ( 'NONE', *, *, #6796, .T. ) ;
#715=FACE_OUTER_BOUND ( 'NONE', #6738, .T. ) ;
#733=CARTESIAN_POINT ( 'NONE',  ( 0.5700000000000001732, -28.49429942988597020, -3.000000000000000000 ) ) ;
#736=VERTEX_POINT ( 'NONE', #2149 ) ;
#737=AXIS2_PLACEMENT_3D ( 'NONE', #7008, #6455, #5943 ) ;
#747=ADVANCED_FACE ( 'NONE', ( #5569 ), #317, .T. ) ;
#761=DIRECTION ( 'NONE',  ( 0.000000000000000000, 0.000000000000000000, 1.000000000000000000 ) ) ;
#768=EDGE_CURVE ( 'NONE', #3595, #3008, #6005, .T. ) ;
#781=ORIENTED_EDGE ( 'NONE', *, *, #6160, .T. ) ;
#788=ORIENTED_EDGE ( 'NONE', *, *, #5777, .T. ) ;
#793=CARTESIAN_POINT ( 'NONE',  ( 0.000000000000000000, 1.484218055610305731, 0.000000000000000000 ) ) ;
#794=EDGE_CURVE ( 'NONE', #502, #2536, #6762, .T. ) ;
#824=ORIENTED_EDGE ( 'NONE', *, *, #453, .T. ) ;
#825=ORIENTED_EDGE ( 'NONE', *, *, #3237, .T. ) ;
#826=UNCERTAINTY_MEASURE_WITH_UNIT (LENGTH_MEASURE( 1.000000000000000082E-05 ), #6861, 'distance_accuracy_value', 'NONE');
#851=EDGE_LOOP ( 'NONE', ( #1261, #352, #7402, #945 ) ) ;
#857=DIRECTION ( 'NONE',  ( 0.000000000000000000, 0.000000000000000000, 1.000000000000000000 ) ) ;
#858=ORIENTED_EDGE ( 'NONE', *, *, #4809, .F. ) ;
#864=CYLINDRICAL_SURFACE ( 'NONE', #2265, 32.81578194438969120 ) ;
#872=AXIS2_PLACEMENT_3D ( 'NONE', #6824, #1256, #1293 ) ;
#877=CARTESIAN_POINT ( 'NONE',  ( -5.238334947888650284, -36.57199107895616663, -3.000000000000000000 ) ) ;
#879=CARTESIAN_POINT ( 'NONE',  ( 5.459126460941064352, -34.89491303563345070, -3.000000000000000000 ) ) ;
#901=ADVANCED_FACE ( 'NONE', ( #434 ), #6948, .F. ) ;
#910=AXIS2_PLACEMENT_3D ( 'NONE', #1832, #6638, #1226 ) ;
#918=FACE_OUTER_BOUND ( 'NONE', #7720, .T. ) ;
#942=ADVANCED_FACE ( 'NONE', ( #4578 ), #355, .T. ) ;
#945=ORIENTED_EDGE ( 'NONE', *, *, #5584, .T. ) ;
#956=PLANE ( 'NONE',  #1181 ) ;
#958=CARTESIAN_POINT ( 'NONE',  ( 2.750000000000000000, -33.63777638310832430, -3.000000000000000000 ) ) ;
#974=AXIS2_PLACEMENT_3D ( 'NONE', #1068, #986, #3480 ) ;
#984=DIRECTION ( 'NONE',  ( 0.000000000000000000, 0.000000000000000000, 1.000000000000000000 ) ) ;
#986=DIRECTION ( 'NONE',  ( 0.000000000000000000, 0.000000000000000000, 1.000000000000000000 ) ) ;
#990=AXIS2_PLACEMENT_3D ( 'NONE', #4722, #1412, #6541 ) ;
#1002=ORIENTED_EDGE ( 'NONE', *, *, #4941, .F. ) ;
#1009=CARTESIAN_POINT ( 'NONE',  ( 4.494751301858288528, -36.47409643479112162, -3.000000000000000000 ) ) ;
#1010=CARTESIAN_POINT ( 'NONE',  ( 0.000000000000000000, 1.484218055610305731, -3.000000000000000000 ) ) ;
#1014=ORIENTED_EDGE ( 'NONE', *, *, #6400, .T. ) ;
#1018=DIRECTION ( 'NONE',  ( -0.000000000000000000, -0.000000000000000000, -1.000000000000000000 ) ) ;
#1028=DIRECTION ( 'NONE',  ( 0.01999999999999999001, -0.9997999799959990108, 0.000000000000000000 ) ) ;
#1034=EDGE_LOOP ( 'NONE', ( #2693, #2711, #5172, #4955 ) ) ;
#1062=CARTESIAN_POINT ( 'NONE',  ( 0.7499999999999730216, -37.49249924984995630, -3.000000000000000000 ) ) ;
#1064=CIRCLE ( 'NONE', #5224, 32.81578194438969120 ) ;
#1068=CARTESIAN_POINT ( 'NONE',  ( 0.000000000000000000, 0.000000000000000000, 0.000000000000000000 ) ) ;
#1072=CYLINDRICAL_SURFACE ( 'NONE', #5378, 32.81578194438969120 ) ;
#1081=AXIS2_PLACEMENT_3D ( 'NONE', #4060, #5924, #4025 ) ;
#1089=DIRECTION ( 'NONE',  ( 0.000000000000000000, 0.000000000000000000, 1.000000000000000000 ) ) ;
#1112=FACE_BOUND ( 'NONE', #2728, .T. ) ;
#1133=EDGE_LOOP ( 'NONE', ( #5984, #5197, #2414, #4649 ) ) ;
#1142=VECTOR ( 'NONE', #5553, 1000.000000000000000 ) ;
#1155=CARTESIAN_POINT ( 'NONE',  ( 0.000000000000000000, 0.000000000000000000, 0.000000000000000000 ) ) ;
#1156=FACE_OUTER_BOUND ( 'NONE', #4453, .T. ) ;
#1167=DIRECTION ( 'NONE',  ( 0.000000000000000000, 0.000000000000000000, 1.000000000000000000 ) ) ;
#1181=AXIS2_PLACEMENT_3D ( 'NONE', #4034, #328, #5851 ) ;
#1188=DIRECTION ( 'NONE',  ( 0.1305261922200541547, 0.9914448613738101601, 0.000000000000000000 ) ) ;
#1189=CYLINDRICAL_SURFACE ( 'NONE', #910, 6.099504629071904382 ) ;
#1196=LINE ( 'NONE', #5321, #3108 ) ;
#1220=APPLICATION_CONTEXT ( 'automotive_design' ) ;
#1226=DIRECTION ( 'NONE',  ( 1.000000000000000000, 0.000000000000000000, 0.000000000000000000 ) ) ;
#1235=CARTESIAN_POINT ( 'NONE',  ( 32.81578194438969120, 1.484218055610305731, -3.000000000000000000 ) ) ;
#1237=DIRECTION ( 'NONE',  ( 0.000000000000000000, 0.000000000000000000, 1.000000000000000000 ) ) ;
#1250=ADVANCED_FACE ( 'NONE', ( #6954 ), #1072, .T. ) ;
#1256=DIRECTION ( 'NONE',  ( 0.000000000000000000, 0.000000000000000000, 1.000000000000000000 ) ) ;
#1261=ORIENTED_EDGE ( 'NONE', *, *, #3237, .F. ) ;
#1262=AXIS2_PLACEMENT_3D ( 'NONE', #5714, #308, #4417 ) ;
#1268=ORIENTED_EDGE ( 'NONE', *, *, #6226, .T. ) ;
#1274=DIRECTION ( 'NONE',  ( 0.01999999999999999001, 0.9997999799959990108, -0.000000000000000000 ) ) ;
#1276=EDGE_CURVE ( 'NONE', #3299, #5007, #5850, .T. ) ;
#1277=ADVANCED_FACE ( 'NONE', ( #3524, #1112, #4068 ), #2899, .F. ) ;
#1293=DIRECTION ( 'NONE',  ( 1.000000000000000000, 0.000000000000000000, 0.000000000000000000 ) ) ;
#1301=CARTESIAN_POINT ( 'NONE',  ( 0.000000000000000000, 0.000000000000000000, 0.000000000000000000 ) ) ;
#1305=ORIENTED_EDGE ( 'NONE', *, *, #6977, .T. ) ;
#1307=CIRCLE ( 'NONE', #4580, 1.250000000000000444 ) ;
#1314=LINE ( 'NONE', #5461, #3554 ) ;
#1340=AXIS2_PLACEMENT_3D ( 'NONE', #5296, #3370, #2237 ) ;
#1378=CARTESIAN_POINT ( 'NONE',  ( 1.499999999999999334, -33.63777638310832430, -3.000000000000000000 ) ) ;
#1386=ADVANCED_FACE ( 'NONE', ( #7713 ), #4719, .T. ) ;
#1404=ORIENTED_EDGE ( 'NONE', *, *, #5880, .F. ) ;
#1412=DIRECTION ( 'NONE',  ( 0.000000000000000000, 0.000000000000000000, 1.000000000000000000 ) ) ;
#1438=DIRECTION ( 'NONE',  ( 0.000000000000000000, 0.000000000000000000, 1.000000000000000000 ) ) ;
#1449=CARTESIAN_POINT ( 'NONE',  ( -1.499999999999999334, -33.63777638310832430, 0.000000000000000000 ) ) ;
#1453=PRODUCT ( 'circlip for shafts heavy_din_Circlip DIN 471 - 60 x 3', 'circlip for shafts heavy_din_Circlip DIN 471 - 60 x 3', '', ( #5587 ) ) ;
#1455=ORIENTED_EDGE ( 'NONE', *, *, #4024, .T. ) ;
#1461=AXIS2_PLACEMENT_3D ( 'NONE', #5654, #7541, #3255 ) ;
#1463=ORIENTED_EDGE ( 'NONE', *, *, #3212, .F. ) ;
#1468=CARTESIAN_POINT ( 'NONE',  ( 5.459126460941067016, -34.89491303563345070, 0.000000000000000000 ) ) ;
#1487=EDGE_LOOP ( 'NONE', ( #7576, #3858, #7591, #1404 ) ) ;
#1491=DIRECTION ( 'NONE',  ( 1.000000000000000000, 0.000000000000000000, 0.000000000000000000 ) ) ;
#1499=AXIS2_PLACEMENT_3D ( 'NONE', #487, #5814, #4631 ) ;
#1500=FACE_OUTER_BOUND ( 'NONE', #7185, .T. ) ;
#1509=EDGE_LOOP ( 'NONE', ( #3965, #7043, #5591, #1455 ) ) ;
#1513=FACE_BOUND ( 'NONE', #7758, .T. ) ;
#1532=VERTEX_POINT ( 'NONE', #5543 ) ;
#1534=ORIENTED_EDGE ( 'NONE', *, *, #4067, .T. ) ;
#1537=VECTOR ( 'NONE', #1237, 1000.000000000000000 ) ;
#1554=DIRECTION ( 'NONE',  ( 1.000000000000000000, 0.000000000000000000, 0.000000000000000000 ) ) ;
#1556=DIRECTION ( 'NONE',  ( 1.000000000000000000, 0.000000000000000000, 0.000000000000000000 ) ) ;
#1593=( NAMED_UNIT ( * ) SI_UNIT ( $, .STERADIAN. ) SOLID_ANGLE_UNIT ( ) );
#1595=CARTESIAN_POINT ( 'NONE',  ( 2.750000000000000000, -33.63777638310832430, -3.000000000000000000 ) ) ;
#1606=FACE_OUTER_BOUND ( 'NONE', #1487, .T. ) ;
#1607=AXIS2_PLACEMENT_3D ( 'NONE', #1912, #4863, #169 ) ;
#1611=VERTEX_POINT ( 'NONE', #63 ) ;
#1612=AXIS2_PLACEMENT_3D ( 'NONE', #11, #5374, #1188 ) ;
#1630=EDGE_LOOP ( 'NONE', ( #5952, #7300, #6677, #6036 ) ) ;
#1659=CARTESIAN_POINT ( 'NONE',  ( -0.5700000000000001732, -28.49429942988597020, 0.000000000000000000 ) ) ;
#1667=ORIENTED_EDGE ( 'NONE', *, *, #1731, .F. ) ;
#1668=EDGE_CURVE ( 'NONE', #2714, #2100, #3369, .T. ) ;
#1676=CARTESIAN_POINT ( 'NONE',  ( 0.000000000000000000, 0.000000000000000000, -3.000000000000000000 ) ) ;
#1706=DIRECTION ( 'NONE',  ( 1.000000000000000000, 0.000000000000000000, 0.000000000000000000 ) ) ;
#1715=LINE ( 'NONE', #4705, #5601 ) ;
#1731=EDGE_CURVE ( 'NONE', #6982, #2714, #5123, .T. ) ;
#1742=ADVANCED_FACE ( 'NONE', ( #330 ), #6850, .F. ) ;
#1755=AXIS2_PLACEMENT_3D ( 'NONE', #1010, #417, #2837 ) ;
#1764=DIRECTION ( 'NONE',  ( 0.000000000000000000, 0.000000000000000000, 1.000000000000000000 ) ) ;
#1780=EDGE_CURVE ( 'NONE', #5051, #371, #7019, .T. ) ;
#1781=ORIENTED_EDGE ( 'NONE', *, *, #453, .F. ) ;
#1783=VECTOR ( 'NONE', #3241, 1000.000000000000000 ) ;
#1795=EDGE_LOOP ( 'NONE', ( #6378, #2655, #4106, #3165 ) ) ;
#1797=ORIENTED_EDGE ( 'NONE', *, *, #32, .T. ) ;
#1800=LINE ( 'NONE', #527, #2639 ) ;
#1810=DIRECTION ( 'NONE',  ( 1.000000000000000000, 0.000000000000000000, 0.000000000000000000 ) ) ;
#1832=CARTESIAN_POINT ( 'NONE',  ( 11.50644898236017433, -35.69105814929478981, -3.000000000000000000 ) ) ;
#1835=EDGE_CURVE ( 'NONE', #1985, #1532, #2381, .T. ) ;
#1842=ADVANCED_FACE ( 'NONE', ( #5853 ), #4444, .F. ) ;
#1850=CARTESIAN_POINT ( 'NONE',  ( -4.586480920263581673, -37.21846574978686562, -3.000000000000000000 ) ) ;
#1864=ADVANCED_FACE ( 'NONE', ( #1156 ), #528, .F. ) ;
#1908=CIRCLE ( 'NONE', #6319, 28.49999999999999645 ) ;
#1912=CARTESIAN_POINT ( 'NONE',  ( 0.000000000000000000, 0.000000000000000000, -3.000000000000000000 ) ) ;
#1924=DIRECTION ( 'NONE',  ( 0.000000000000000000, 0.000000000000000000, 1.000000000000000000 ) ) ;
#1943=LINE ( 'NONE', #3087, #58 ) ;
#1957=CARTESIAN_POINT ( 'NONE',  ( -1.499999999999999334, -33.63777638310832430, -3.000000000000000000 ) ) ;
#1969=CARTESIAN_POINT ( 'NONE',  ( 4.000000000000000000, -33.63777638310832430, 0.000000000000000000 ) ) ;
#1977=( GEOMETRIC_REPRESENTATION_CONTEXT ( 3 ) GLOBAL_UNCERTAINTY_ASSIGNED_CONTEXT ( ( #6684 ) ) GLOBAL_UNIT_ASSIGNED_CONTEXT ( ( #2818, #4151, #1593 ) ) REPRESENTATION_CONTEXT ( 'NONE', 'WORKASPACE' ) );
#1979=( LENGTH_UNIT ( ) NAMED_UNIT ( * ) SI_UNIT ( .MILLI., .METRE. ) );
#1981=EDGE_CURVE ( 'NONE', #4626, #5051, #647, .T. ) ;
#1984=AXIS2_PLACEMENT_3D ( 'NONE', #4385, #5723, #3176 ) ;
#1985=VERTEX_POINT ( 'NONE', #3725 ) ;
#1995=DIRECTION ( 'NONE',  ( 0.1305261922200541547, 0.9914448613738101601, -0.000000000000000000 ) ) ;
#2014=CARTESIAN_POINT ( 'NONE',  ( 0.000000000000000000, 0.000000000000000000, -3.000000000000000000 ) ) ;
#2016=SURFACE_SIDE_STYLE ('',( #4527 ) ) ;
#2017=EDGE_CURVE ( 'NONE', #2536, #3380, #2513, .T. ) ;
#2020=ADVANCED_FACE ( 'NONE', ( #3059 ), #5459, .F. ) ;
#2035=DIRECTION ( 'NONE',  ( 1.000000000000000000, 0.000000000000000000, 0.000000000000000000 ) ) ;
#2039=AXIS2_PLACEMENT_3D ( 'NONE', #2456, #4843, #7256 ) ;
#2054=DIRECTION ( 'NONE',  ( 0.000000000000000000, 0.000000000000000000, 1.000000000000000000 ) ) ;
#2061=EDGE_CURVE ( 'NONE', #7599, #4081, #1943, .T. ) ;
#2073=DIRECTION ( 'NONE',  ( 0.000000000000000000, 0.000000000000000000, 1.000000000000000000 ) ) ;
#2091=AXIS2_PLACEMENT_3D ( 'NONE', #611, #648, #56 ) ;
#2093=ORIENTED_EDGE ( 'NONE', *, *, #7116, .F. ) ;
#2094=DIRECTION ( 'NONE',  ( 0.000000000000000000, 0.000000000000000000, 1.000000000000000000 ) ) ;
#2100=VERTEX_POINT ( 'NONE', #5496 ) ;
#2101=ORIENTED_EDGE ( 'NONE', *, *, #4995, .T. ) ;
#2102=CIRCLE ( 'NONE', #5874, 28.49999999999999645 ) ;
#2105=DIRECTION ( 'NONE',  ( 1.000000000000000000, 0.000000000000000000, 0.000000000000000000 ) ) ;
#2110=EDGE_CURVE ( 'NONE', #5113, #3517, #476, .T. ) ;
#2114=DIRECTION ( 'NONE',  ( -0.000000000000000000, -0.000000000000000000, -1.000000000000000000 ) ) ;
#2149=CARTESIAN_POINT ( 'NONE',  ( -9.702951051037022268, -29.86427928513813512, -3.000000000000000000 ) ) ;
#2167=EDGE_CURVE ( 'NONE', #3380, #7398, #5515, .T. ) ;
#2168=DIRECTION ( 'NONE',  ( 1.000000000000000000, 0.000000000000000000, 0.000000000000000000 ) ) ;
#2175=EDGE_CURVE ( 'NONE', #371, #5113, #5687, .T. ) ;
#2191=ORIENTED_EDGE ( 'NONE', *, *, #4809, .T. ) ;
#2224=EDGE_CURVE ( 'NONE', #545, #371, #6950, .T. ) ;
#2234=ORIENTED_EDGE ( 'NONE', *, *, #463, .F. ) ;
#2237=DIRECTION ( 'NONE',  ( 1.000000000000000000, 0.000000000000000000, -0.000000000000000000 ) ) ;
#2265=AXIS2_PLACEMENT_3D ( 'NONE', #3317, #7568, #2105 ) ;
#2281=DIRECTION ( 'NONE',  ( 0.000000000000000000, 0.000000000000000000, 1.000000000000000000 ) ) ;
#2306=SHAPE_REPRESENTATION ( 'circlip for shafts heavy_din_Circlip DIN 471 - 60 x 3', ( #7485 ), #6367 ) ;
#2352=ADVANCED_FACE ( 'NONE', ( #3989 ), #2773, .F. ) ;
#2362=EDGE_CURVE ( 'NONE', #5007, #5051, #5898, .T. ) ;
#2363=CARTESIAN_POINT ( 'NONE',  ( 0.5700000000000001732, -28.49429942988597020, -3.000000000000000000 ) ) ;
#2365=ORIENTED_EDGE ( 'NONE', *, *, #5920, .T. ) ;
#2373=FACE_OUTER_BOUND ( 'NONE', #2769, .T. ) ;
#2381=CIRCLE ( 'NONE', #3250, 37.50000000000000000 ) ;
#2410=DIRECTION ( 'NONE',  ( 0.000000000000000000, 0.000000000000000000, 1.000000000000000000 ) ) ;
#2414=ORIENTED_EDGE ( 'NONE', *, *, #4941, .T. ) ;
#2422=ADVANCED_FACE ( 'NONE', ( #715 ), #6006, .T. ) ;
#2438=LINE ( 'NONE', #7240, #7211 ) ;
#2447=CARTESIAN_POINT ( 'NONE',  ( 1.499999999999999334, -33.63777638310832430, -3.000000000000000000 ) ) ;
#2456=CARTESIAN_POINT ( 'NONE',  ( 11.50644898236017433, -35.69105814929478981, -3.000000000000000000 ) ) ;
#2461=EDGE_CURVE ( 'NONE', #1532, #2556, #2470, .T. ) ;
#2468=AXIS2_PLACEMENT_3D ( 'NONE', #6852, #1438, #7078 ) ;
#2470=LINE ( 'NONE', #3638, #227 ) ;
#2482=CARTESIAN_POINT ( 'NONE',  ( 5.459126460941064352, -34.89491303563345070, -3.000000000000000000 ) ) ;
#2495=CARTESIAN_POINT ( 'NONE',  ( -5.459126460941067016, -34.89491303563345070, -3.000000000000000000 ) ) ;
#2512=DIRECTION ( 'NONE',  ( 1.000000000000000000, 0.000000000000000000, 0.000000000000000000 ) ) ;
#2513=LINE ( 'NONE', #1235, #7025 ) ;
#2536=VERTEX_POINT ( 'NONE', #7305 ) ;
#2556=VERTEX_POINT ( 'NONE', #3169 ) ;
#2566=ORIENTED_EDGE ( 'NONE', *, *, #794, .F. ) ;
#2575=EDGE_LOOP ( 'NONE', ( #1667, #7727, #5992, #418 ) ) ;
#2583=DIRECTION ( 'NONE',  ( 1.000000000000000000, 0.000000000000000000, 0.000000000000000000 ) ) ;
#2587=VECTOR ( 'NONE', #2410, 1000.000000000000000 ) ;
#2601=DIRECTION ( 'NONE',  ( 0.000000000000000000, 0.000000000000000000, 1.000000000000000000 ) ) ;
#2639=VECTOR ( 'NONE', #1764, 1000.000000000000000 ) ;
#2641=DIRECTION ( 'NONE',  ( -0.000000000000000000, -0.000000000000000000, -1.000000000000000000 ) ) ;
#2642=CARTESIAN_POINT ( 'NONE',  ( 0.5700000000000001732, -28.49429942988597020, 0.000000000000000000 ) ) ;
#2643=( NAMED_UNIT ( * ) SI_UNIT ( $, .STERADIAN. ) SOLID_ANGLE_UNIT ( ) );
#2655=ORIENTED_EDGE ( 'NONE', *, *, #2868, .F. ) ;
#2658=DIRECTION ( 'NONE',  ( 0.9997999799959990108, -0.01999999999999999001, 0.000000000000000000 ) ) ;
#2666=CARTESIAN_POINT ( 'NONE',  ( 0.000000000000000000, 0.000000000000000000, -3.000000000000000000 ) ) ;
#2683=ADVANCED_FACE ( 'NONE', ( #1606 ), #4011, .T. ) ;
#2693=ORIENTED_EDGE ( 'NONE', *, *, #6062, .T. ) ;
#2698=DIRECTION ( 'NONE',  ( 0.000000000000000000, 0.000000000000000000, 1.000000000000000000 ) ) ;
#2707=SHAPE_DEFINITION_REPRESENTATION ( #7309, #2306 ) ;
#2711=ORIENTED_EDGE ( 'NONE', *, *, #4964, .T. ) ;
#2713=ORIENTED_EDGE ( 'NONE', *, *, #2886, .F. ) ;
#2714=VERTEX_POINT ( 'NONE', #5991 ) ;
#2715=ORIENTED_EDGE ( 'NONE', *, *, #2110, .F. ) ;
#2728=EDGE_LOOP ( 'NONE', ( #2191, #4250 ) ) ;
#2765=AXIS2_PLACEMENT_3D ( 'NONE', #1155, #646, #2512 ) ;
#2769=EDGE_LOOP ( 'NONE', ( #30, #6012, #393, #5861 ) ) ;
#2773=CYLINDRICAL_SURFACE ( 'NONE', #4819, 28.49999999999999645 ) ;
#2782=LINE ( 'NONE', #3960, #3329 ) ;
#2784=DIRECTION ( 'NONE',  ( 0.000000000000000000, 0.000000000000000000, 1.000000000000000000 ) ) ;
#2786=ADVANCED_FACE ( 'NONE', ( #4047 ), #500, .F. ) ;
#2806=DIRECTION ( 'NONE',  ( 1.000000000000000000, 0.000000000000000000, 0.000000000000000000 ) ) ;
#2807=EDGE_LOOP ( 'NONE', ( #4118, #858, #6624, #1797 ) ) ;
#2818=( LENGTH_UNIT ( ) NAMED_UNIT ( * ) SI_UNIT ( .MILLI., .METRE. ) );
#2823=CARTESIAN_POINT ( 'NONE',  ( 0.000000000000000000, 1.484218055610305731, -3.000000000000000000 ) ) ;
#2831=VECTOR ( 'NONE', #7286, 999.9999999999998863 ) ;
#2837=DIRECTION ( 'NONE',  ( 1.000000000000000000, 0.000000000000000000, 0.000000000000000000 ) ) ;
#2839=ORIENTED_EDGE ( 'NONE', *, *, #2061, .T. ) ;
#2859=FACE_BOUND ( 'NONE', #4066, .T. ) ;
#2868=EDGE_CURVE ( 'NONE', #1985, #2714, #656, .T. ) ;
#2886=EDGE_CURVE ( 'NONE', #6434, #3299, #4322, .T. ) ;
#2899=PLANE ( 'NONE',  #1340 ) ;
#2920=DIRECTION ( 'NONE',  ( 0.1305261922200541547, 0.9914448613738101601, -0.000000000000000000 ) ) ;
#2952=CARTESIAN_POINT ( 'NONE',  ( -5.459126460941067016, -34.89491303563345070, -3.000000000000000000 ) ) ;
#2959=EDGE_LOOP ( 'NONE', ( #1002, #4901, #156, #5767 ) ) ;
#2990=ORIENTED_EDGE ( 'NONE', *, *, #5576, .T. ) ;
#3001=VERTEX_POINT ( 'NONE', #1969 ) ;
#3008=VERTEX_POINT ( 'NONE', #216 ) ;
#3047=DIRECTION ( 'NONE',  ( -0.000000000000000000, -0.000000000000000000, -1.000000000000000000 ) ) ;
#3059=FACE_OUTER_BOUND ( 'NONE', #5067, .T. ) ;
#3076=CIRCLE ( 'NONE', #4329, 6.099504629071905271 ) ;
#3083=ORIENTED_EDGE ( 'NONE', *, *, #4067, .F. ) ;
#3086=FACE_OUTER_BOUND ( 'NONE', #1509, .T. ) ;
#3087=CARTESIAN_POINT ( 'NONE',  ( -28.49999999999999645, 3.490243377569956456E-15, -3.000000000000000000 ) ) ;
#3090=DIRECTION ( 'NONE',  ( 0.01999999999999999001, 0.9997999799959990108, -0.000000000000000000 ) ) ;
#3099=LINE ( 'NONE', #5495, #234 ) ;
#3108=VECTOR ( 'NONE', #603, 1000.000000000000000 ) ;
#3109=CARTESIAN_POINT ( 'NONE',  ( -5.459126460941067016, -34.89491303563345070, 0.000000000000000000 ) ) ;
#3146=AXIS2_PLACEMENT_3D ( 'NONE', #1595, #3488, #7038 ) ;
#3153=VERTEX_POINT ( 'NONE', #151 ) ;
#3165=ORIENTED_EDGE ( 'NONE', *, *, #7647, .T. ) ;
#3169=CARTESIAN_POINT ( 'NONE',  ( -0.5700000000000001732, -28.49429942988597020, -3.000000000000000000 ) ) ;
#3176=DIRECTION ( 'NONE',  ( 1.000000000000000000, 0.000000000000000000, 0.000000000000000000 ) ) ;
#3188=DIRECTION ( 'NONE',  ( 0.000000000000000000, 0.000000000000000000, 1.000000000000000000 ) ) ;
#3189=VECTOR ( 'NONE', #5540, 1000.000000000000000 ) ;
#3194=CARTESIAN_POINT ( 'NONE',  ( 0.000000000000000000, 0.000000000000000000, -3.000000000000000000 ) ) ;
#3212=EDGE_CURVE ( 'NONE', #7629, #1985, #242, .T. ) ;
#3237=EDGE_CURVE ( 'NONE', #7233, #6072, #4487, .T. ) ;
#3241=DIRECTION ( 'NONE',  ( 0.000000000000000000, 0.000000000000000000, 1.000000000000000000 ) ) ;
#3245=ORIENTED_EDGE ( 'NONE', *, *, #1276, .F. ) ;
#3247=DIRECTION ( 'NONE',  ( 0.000000000000000000, 0.000000000000000000, 1.000000000000000000 ) ) ;
#3250=AXIS2_PLACEMENT_3D ( 'NONE', #1676, #7706, #4632 ) ;
#3255=DIRECTION ( 'NONE',  ( 1.000000000000000000, 0.000000000000000000, 0.000000000000000000 ) ) ;
#3291=AXIS2_PLACEMENT_3D ( 'NONE', #6229, #2094, #6342 ) ;
#3299=VERTEX_POINT ( 'NONE', #2642 ) ;
#3306=FILL_AREA_STYLE_COLOUR ( '', #5099 ) ;
#3311=ORIENTED_EDGE ( 'NONE', *, *, #3974, .T. ) ;
#3312=VERTEX_POINT ( 'NONE', #1449 ) ;
#3317=CARTESIAN_POINT ( 'NONE',  ( 0.000000000000000000, 1.484218055610305731, -3.000000000000000000 ) ) ;
#3319=CIRCLE ( 'NONE', #546, 28.49999999999999645 ) ;
#3320=VERTEX_POINT ( 'NONE', #6972 ) ;
#3321=DIRECTION ( 'NONE',  ( 0.01999999999999999001, 0.9997999799959990108, 0.000000000000000000 ) ) ;
#3324=CARTESIAN_POINT ( 'NONE',  ( 11.50644898236017433, -35.69105814929478981, 0.000000000000000000 ) ) ;
#3329=VECTOR ( 'NONE', #4666, 1000.000000000000000 ) ;
#3334=DIRECTION ( 'NONE',  ( 1.000000000000000000, 0.000000000000000000, 0.000000000000000000 ) ) ;
#3342=ORIENTED_EDGE ( 'NONE', *, *, #5880, .T. ) ;
#3369=CIRCLE ( 'NONE', #4879, 37.50000000000000000 ) ;
#3370=DIRECTION ( 'NONE',  ( 0.000000000000000000, 0.000000000000000000, 1.000000000000000000 ) ) ;
#3375=DIRECTION ( 'NONE',  ( 0.000000000000000000, 0.000000000000000000, 1.000000000000000000 ) ) ;
#3379=VECTOR ( 'NONE', #2698, 1000.000000000000000 ) ;
#3380=VERTEX_POINT ( 'NONE', #6596 ) ;
#3430=CARTESIAN_POINT ( 'NONE',  ( -5.238334947888650284, -36.57199107895616663, 0.000000000000000000 ) ) ;
#3433=ORIENTED_EDGE ( 'NONE', *, *, #610, .T. ) ;
#3436=DIRECTION ( 'NONE',  ( 0.000000000000000000, 0.000000000000000000, 1.000000000000000000 ) ) ;
#3447=CARTESIAN_POINT ( 'NONE',  ( -2.750000000000000000, -33.63777638310832430, -3.000000000000000000 ) ) ;
#3453=ORIENTED_EDGE ( 'NONE', *, *, #5920, .F. ) ;
#3476=MECHANICAL_DESIGN_GEOMETRIC_PRESENTATION_REPRESENTATION('',(#3729),#1977);
#3477=DIRECTION ( 'NONE',  ( 1.000000000000000000, 0.000000000000000000, 0.000000000000000000 ) ) ;
#3480=DIRECTION ( 'NONE',  ( 1.000000000000000000, 0.000000000000000000, 0.000000000000000000 ) ) ;
#3485=DIRECTION ( 'NONE',  ( 0.000000000000000000, 0.000000000000000000, 1.000000000000000000 ) ) ;
#3488=DIRECTION ( 'NONE',  ( 0.000000000000000000, 0.000000000000000000, 1.000000000000000000 ) ) ;
#3491=ORIENTED_EDGE ( 'NONE', *, *, #6400, .F. ) ;
#3498=DIRECTION ( 'NONE',  ( -0.9914448613738101601, -0.1305261922200541547, 0.000000000000000000 ) ) ;
#3517=VERTEX_POINT ( 'NONE', #7264 ) ;
#3524=FACE_BOUND ( 'NONE', #3826, .T. ) ;
#3541=CARTESIAN_POINT ( 'NONE',  ( 0.000000000000000000, 0.000000000000000000, -3.000000000000000000 ) ) ;
#3554=VECTOR ( 'NONE', #7159, 1000.000000000000000 ) ;
#3587=CARTESIAN_POINT ( 'NONE',  ( 2.750000000000000000, -33.63777638310832430, 0.000000000000000000 ) ) ;
#3595=VERTEX_POINT ( 'NONE', #1378 ) ;
#3613=ADVANCED_FACE ( 'NONE', ( #3086 ), #83, .F. ) ;
#3628=ORIENTED_EDGE ( 'NONE', *, *, #1835, .F. ) ;
#3637=CIRCLE ( 'NONE', #6793, 32.81578194438969120 ) ;
#3638=CARTESIAN_POINT ( 'NONE',  ( -0.5700000000000001732, -28.49429942988597020, -3.000000000000000000 ) ) ;
#3688=AXIS2_PLACEMENT_3D ( 'NONE', #2952, #3498, #454 ) ;
#3694=EDGE_CURVE ( 'NONE', #6870, #3153, #12, .T. ) ;
#3709=AXIS2_PLACEMENT_3D ( 'NONE', #1009, #1089, #4762 ) ;
#3725=CARTESIAN_POINT ( 'NONE',  ( -4.586480920263581673, -37.21846574978686562, -3.000000000000000000 ) ) ;
#3727=AXIS2_PLACEMENT_3D ( 'NONE', #4524, #7555, #2168 ) ;
#3729=STYLED_ITEM('',(#7830),#475);
#3747=EDGE_CURVE ( 'NONE', #2556, #6929, #6236, .T. ) ;
#3749=AXIS2_PLACEMENT_3D ( 'NONE', #958, #3375, #3334 ) ;
#3758=DIRECTION ( 'NONE',  ( 0.000000000000000000, 0.000000000000000000, 1.000000000000000000 ) ) ;
#3781=ORIENTED_EDGE ( 'NONE', *, *, #1276, .T. ) ;
#3785=CARTESIAN_POINT ( 'NONE',  ( -11.50644898236017433, -35.69105814929478981, -3.000000000000000000 ) ) ;
#3815=LINE ( 'NONE', #4439, #4971 ) ;
#3826=EDGE_LOOP ( 'NONE', ( #5228, #1014 ) ) ;
#3846=MECHANICAL_DESIGN_GEOMETRIC_PRESENTATION_REPRESENTATION('',(#5856),#4725);
#3858=ORIENTED_EDGE ( 'NONE', *, *, #2017, .T. ) ;
#3864=CARTESIAN_POINT ( 'NONE',  ( -2.750000000000000000, -33.63777638310832430, 0.000000000000000000 ) ) ;
#3884=CARTESIAN_POINT ( 'NONE',  ( 9.702951051037011609, -29.86427928513813868, -3.000000000000000000 ) ) ;
#3891=DIRECTION ( 'NONE',  ( 0.000000000000000000, 0.000000000000000000, 1.000000000000000000 ) ) ;
#3894=ORIENTED_EDGE ( 'NONE', *, *, #1780, .T. ) ;
#3937=EDGE_CURVE ( 'NONE', #545, #4638, #505, .T. ) ;
#3953=CARTESIAN_POINT ( 'NONE',  ( 5.238334947888644955, -36.57199107895616663, -3.000000000000000000 ) ) ;
#3959=CARTESIAN_POINT ( 'NONE',  ( 0.7499999999999730216, -37.49249924984995630, -3.000000000000000000 ) ) ;
#3960=CARTESIAN_POINT ( 'NONE',  ( -0.7500000000000000000, -37.49249924984995630, -3.000000000000000000 ) ) ;
#3965=ORIENTED_EDGE ( 'NONE', *, *, #3694, .F. ) ;
#3974=EDGE_CURVE ( 'NONE', #1611, #3001, #4922, .T. ) ;
#3982=AXIS2_PLACEMENT_3D ( 'NONE', #4426, #3247, #2583 ) ;
#3989=FACE_OUTER_BOUND ( 'NONE', #2959, .T. ) ;
#3991=ORIENTED_EDGE ( 'NONE', *, *, #6887, .F. ) ;
#3993=CARTESIAN_POINT ( 'NONE',  ( 0.000000000000000000, 1.484218055610305731, -3.000000000000000000 ) ) ;
#3995=AXIS2_PLACEMENT_3D ( 'NONE', #793, #2073, #6247 ) ;
#4004=ORIENTED_EDGE ( 'NONE', *, *, #2362, .F. ) ;
#4006=CIRCLE ( 'NONE', #737, 28.49999999999999645 ) ;
#4010=DIRECTION ( 'NONE',  ( 1.000000000000000000, 0.000000000000000000, 0.000000000000000000 ) ) ;
#4011=CYLINDRICAL_SURFACE ( 'NONE', #1755, 32.81578194438969120 ) ;
#4024=EDGE_CURVE ( 'NONE', #7389, #3153, #1, .T. ) ;
#4025=DIRECTION ( 'NONE',  ( 1.000000000000000000, 0.000000000000000000, 0.000000000000000000 ) ) ;
#4034=CARTESIAN_POINT ( 'NONE',  ( 0.000000000000000000, 0.000000000000000000, 0.000000000000000000 ) ) ;
#4047=FACE_OUTER_BOUND ( 'NONE', #1133, .T. ) ;
#4060=CARTESIAN_POINT ( 'NONE',  ( -4.494751301858288528, -36.47409643479112162, -3.000000000000000000 ) ) ;
#4066=EDGE_LOOP ( 'NONE', ( #4773, #7151 ) ) ;
#4067=EDGE_CURVE ( 'NONE', #4638, #502, #5432, .T. ) ;
#4068=FACE_OUTER_BOUND ( 'NONE', #244, .T. ) ;
#4075=DIRECTION ( 'NONE',  ( 1.000000000000000000, 0.000000000000000000, 0.000000000000000000 ) ) ;
#4079=EDGE_LOOP ( 'NONE', ( #3245, #2713, #2365, #6322 ) ) ;
#4081=VERTEX_POINT ( 'NONE', #6702 ) ;
#4097=CARTESIAN_POINT ( 'NONE',  ( -1.499999999999999334, -33.63777638310832430, -3.000000000000000000 ) ) ;
#4106=ORIENTED_EDGE ( 'NONE', *, *, #1835, .T. ) ;
#4118=ORIENTED_EDGE ( 'NONE', *, *, #5777, .F. ) ;
#4138=EDGE_CURVE ( 'NONE', #5285, #6434, #1908, .T. ) ;
#4151=( NAMED_UNIT ( * ) PLANE_ANGLE_UNIT ( ) SI_UNIT ( $, .RADIAN. ) );
#4161=PRODUCT_DEFINITION ( 'UNKNOWN', '', #5069, #4492 ) ;
#4188=CIRCLE ( 'NONE', #5956, 32.81578194438969120 ) ;
#4211=ORIENTED_EDGE ( 'NONE', *, *, #768, .F. ) ;
#4214=DIRECTION ( 'NONE',  ( 1.000000000000000000, 0.000000000000000000, 0.000000000000000000 ) ) ;
#4226=FACE_OUTER_BOUND ( 'NONE', #148, .T. ) ;
#4228=EDGE_CURVE ( 'NONE', #2556, #7599, #7065, .T. ) ;
#4240=EDGE_CURVE ( 'NONE', #6357, #7233, #6694, .T. ) ;
#4250=ORIENTED_EDGE ( 'NONE', *, *, #768, .T. ) ;
#4273=CARTESIAN_POINT ( 'NONE',  ( -4.000000000000000000, -33.63777638310832430, 0.000000000000000000 ) ) ;
#4274=ORIENTED_EDGE ( 'NONE', *, *, #4228, .F. ) ;
#4277=LINE ( 'NONE', #615, #3189 ) ;
#4299=DIRECTION ( 'NONE',  ( 0.000000000000000000, 0.000000000000000000, 1.000000000000000000 ) ) ;
#4307=CARTESIAN_POINT ( 'NONE',  ( 0.7499999999999730216, -37.49249924984995630, 0.000000000000000000 ) ) ;
#4313=ADVANCED_FACE ( 'NONE', ( #4641 ), #5355, .T. ) ;
#4317=EDGE_CURVE ( 'NONE', #6929, #4081, #4006, .T. ) ;
#4322=LINE ( 'NONE', #733, #6291 ) ;
#4323=AXIS2_PLACEMENT_3D ( 'NONE', #7289, #623, #6105 ) ;
#4329=AXIS2_PLACEMENT_3D ( 'NONE', #3785, #3047, #6114 ) ;
#4333=ORIENTED_EDGE ( 'NONE', *, *, #2110, .T. ) ;
#4339=DIRECTION ( 'NONE',  ( 0.000000000000000000, 0.000000000000000000, 1.000000000000000000 ) ) ;
#4369=( NAMED_UNIT ( * ) PLANE_ANGLE_UNIT ( ) SI_UNIT ( $, .RADIAN. ) );
#4383=VECTOR ( 'NONE', #1995, 999.9999999999998863 ) ;
#4385=CARTESIAN_POINT ( 'NONE',  ( 0.000000000000000000, 1.484218055610305731, -3.000000000000000000 ) ) ;
#4417=DIRECTION ( 'NONE',  ( 1.000000000000000000, 0.000000000000000000, 0.000000000000000000 ) ) ;
#4426=CARTESIAN_POINT ( 'NONE',  ( 2.750000000000000000, -33.63777638310832430, -3.000000000000000000 ) ) ;
#4439=CARTESIAN_POINT ( 'NONE',  ( 9.702951051037011609, -29.86427928513813868, -3.000000000000000000 ) ) ;
#4444=CYLINDRICAL_SURFACE ( 'NONE', #6652, 1.250000000000000444 ) ;
#4449=PRESENTATION_STYLE_ASSIGNMENT (( #6786 ) ) ;
#4453=EDGE_LOOP ( 'NONE', ( #4211, #788, #3311, #5307 ) ) ;
#4487=LINE ( 'NONE', #7481, #6049 ) ;
#4492=PRODUCT_DEFINITION_CONTEXT ( 'detailed design', #6770, 'design' ) ;
#4504=VECTOR ( 'NONE', #136, 1000.000000000000000 ) ;
#4505=DIRECTION ( 'NONE',  ( 0.000000000000000000, 0.000000000000000000, 1.000000000000000000 ) ) ;
#4512=EDGE_CURVE ( 'NONE', #7398, #6870, #3637, .T. ) ;
#4521=ORIENTED_EDGE ( 'NONE', *, *, #3747, .F. ) ;
#4524=CARTESIAN_POINT ( 'NONE',  ( 2.750000000000000000, -33.63777638310832430, 0.000000000000000000 ) ) ;
#4527=SURFACE_STYLE_FILL_AREA ( #5555 ) ;
#4545=DIRECTION ( 'NONE',  ( 1.000000000000000000, 0.000000000000000000, 0.000000000000000000 ) ) ;
#4549=CARTESIAN_POINT ( 'NONE',  ( 0.000000000000000000, 0.000000000000000000, 0.000000000000000000 ) ) ;
#4578=FACE_OUTER_BOUND ( 'NONE', #2575, .T. ) ;
#4580=AXIS2_PLACEMENT_3D ( 'NONE', #3864, #857, #1491 ) ;
#4626=VERTEX_POINT ( 'NONE', #7395 ) ;
#4627=ORIENTED_EDGE ( 'NONE', *, *, #2461, .F. ) ;
#4631=DIRECTION ( 'NONE',  ( 1.000000000000000000, 0.000000000000000000, 0.000000000000000000 ) ) ;
#4632=DIRECTION ( 'NONE',  ( 1.000000000000000000, 0.000000000000000000, 0.000000000000000000 ) ) ;
#4636=ORIENTED_EDGE ( 'NONE', *, *, #4228, .T. ) ;
#4638=VERTEX_POINT ( 'NONE', #879 ) ;
#4641=FACE_OUTER_BOUND ( 'NONE', #473, .T. ) ;
#4649=ORIENTED_EDGE ( 'NONE', *, *, #4995, .F. ) ;
#4666=DIRECTION ( 'NONE',  ( 0.000000000000000000, 0.000000000000000000, 1.000000000000000000 ) ) ;
#4673=ORIENTED_EDGE ( 'NONE', *, *, #1731, .T. ) ;
#4693=CARTESIAN_POINT ( 'NONE',  ( -2.750000000000000000, -33.63777638310832430, -3.000000000000000000 ) ) ;
#4705=CARTESIAN_POINT ( 'NONE',  ( -5.459126460941067016, -34.89491303563345070, -3.000000000000000000 ) ) ;
#4719=CYLINDRICAL_SURFACE ( 'NONE', #5887, 37.50000000000000000 ) ;
#4722=CARTESIAN_POINT ( 'NONE',  ( 0.000000000000000000, 0.000000000000000000, -3.000000000000000000 ) ) ;
#4725=( GEOMETRIC_REPRESENTATION_CONTEXT ( 3 ) GLOBAL_UNCERTAINTY_ASSIGNED_CONTEXT ( ( #826 ) ) GLOBAL_UNIT_ASSIGNED_CONTEXT ( ( #6861, #6192, #2643 ) ) REPRESENTATION_CONTEXT ( 'NONE', 'WORKASPACE' ) );
#4762=DIRECTION ( 'NONE',  ( 1.000000000000000000, 0.000000000000000000, 0.000000000000000000 ) ) ;
#4773=ORIENTED_EDGE ( 'NONE', *, *, #32, .F. ) ;
#4775=CIRCLE ( 'NONE', #3146, 1.250000000000000222 ) ;
#4781=ORIENTED_EDGE ( 'NONE', *, *, #1668, .T. ) ;
#4805=ORIENTED_EDGE ( 'NONE', *, *, #5584, .F. ) ;
#4809=EDGE_CURVE ( 'NONE', #3008, #3595, #4775, .T. ) ;
#4819=AXIS2_PLACEMENT_3D ( 'NONE', #517, #3436, #1706 ) ;
#4831=CARTESIAN_POINT ( 'NONE',  ( 0.000000000000000000, 1.484218055610305731, 0.000000000000000000 ) ) ;
#4843=DIRECTION ( 'NONE',  ( -0.000000000000000000, -0.000000000000000000, -1.000000000000000000 ) ) ;
#4857=EDGE_CURVE ( 'NONE', #3320, #736, #7299, .T. ) ;
#4863=DIRECTION ( 'NONE',  ( 0.000000000000000000, 0.000000000000000000, 1.000000000000000000 ) ) ;
#4877=PLANE ( 'NONE',  #4323 ) ;
#4879=AXIS2_PLACEMENT_3D ( 'NONE', #4549, #6926, #7471 ) ;
#4885=AXIS2_PLACEMENT_3D ( 'NONE', #3324, #2114, #2035 ) ;
#4901=ORIENTED_EDGE ( 'NONE', *, *, #4138, .T. ) ;
#4922=CIRCLE ( 'NONE', #7062, 1.250000000000000222 ) ;
#4941=EDGE_CURVE ( 'NONE', #5285, #7680, #1800, .T. ) ;
#4945=VECTOR ( 'NONE', #6468, 1000.000000000000000 ) ;
#4955=ORIENTED_EDGE ( 'NONE', *, *, #2017, .F. ) ;
#4964=EDGE_CURVE ( 'NONE', #3320, #7398, #3099, .T. ) ;
#4969=ORIENTED_EDGE ( 'NONE', *, *, #5338, .F. ) ;
#4971=VECTOR ( 'NONE', #3891, 1000.000000000000000 ) ;
#4983=ORIENTED_EDGE ( 'NONE', *, *, #2175, .T. ) ;
#4995=EDGE_CURVE ( 'NONE', #4081, #7680, #5909, .T. ) ;
#5007=VERTEX_POINT ( 'NONE', #4307 ) ;
#5044=ORIENTED_EDGE ( 'NONE', *, *, #5576, .F. ) ;
#5051=VERTEX_POINT ( 'NONE', #6719 ) ;
#5057=ADVANCED_FACE ( 'NONE', ( #1500 ), #864, .T. ) ;
#5060=CARTESIAN_POINT ( 'NONE',  ( 5.238334947888644955, -36.57199107895616663, 0.000000000000000000 ) ) ;
#5067=EDGE_LOOP ( 'NONE', ( #4636, #2839, #7681, #4521 ) ) ;
#5069=PRODUCT_DEFINITION_FORMATION_WITH_SPECIFIED_SOURCE ( 'ANY', '', #1453, .NOT_KNOWN. ) ;
#5072=DIRECTION ( 'NONE',  ( -0.000000000000000000, -0.000000000000000000, -1.000000000000000000 ) ) ;
#5096=DIRECTION ( 'NONE',  ( 1.000000000000000000, 0.000000000000000000, 0.000000000000000000 ) ) ;
#5099=COLOUR_RGB ( '',1.000000000000000000, 0.9490196078431372140, 0.9098039215686274384 ) ;
#5113=VERTEX_POINT ( 'NONE', #310 ) ;
#5123=CIRCLE ( 'NONE', #6139, 0.7500000000000041078 ) ;
#5141=CARTESIAN_POINT ( 'NONE',  ( 28.49999999999999645, 0.000000000000000000, 0.000000000000000000 ) ) ;
#5147=ORIENTED_EDGE ( 'NONE', *, *, #4317, .T. ) ;
#5151=ORIENTED_EDGE ( 'NONE', *, *, #5761, .F. ) ;
#5172=ORIENTED_EDGE ( 'NONE', *, *, #2167, .F. ) ;
#5179=DIRECTION ( 'NONE',  ( -1.000000000000000000, 0.000000000000000000, 0.000000000000000000 ) ) ;
#5194=FACE_OUTER_BOUND ( 'NONE', #7511, .T. ) ;
#5197=ORIENTED_EDGE ( 'NONE', *, *, #463, .T. ) ;
#5217=ORIENTED_EDGE ( 'NONE', *, *, #2167, .T. ) ;
#5224=AXIS2_PLACEMENT_3D ( 'NONE', #2823, #2281, #1556 ) ;
#5228=ORIENTED_EDGE ( 'NONE', *, *, #4240, .T. ) ;
#5249=LINE ( 'NONE', #1062, #4945 ) ;
#5263=DIRECTION ( 'NONE',  ( 0.000000000000000000, 0.000000000000000000, 1.000000000000000000 ) ) ;
#5283=CARTESIAN_POINT ( 'NONE',  ( 28.49999999999999645, 0.000000000000000000, -3.000000000000000000 ) ) ;
#5285=VERTEX_POINT ( 'NONE', #5283 ) ;
#5295=ORIENTED_EDGE ( 'NONE', *, *, #5761, .T. ) ;
#5296=CARTESIAN_POINT ( 'NONE',  ( 0.000000000000000000, 0.000000000000000000, -3.000000000000000000 ) ) ;
#5307=ORIENTED_EDGE ( 'NONE', *, *, #6169, .F. ) ;
#5321=CARTESIAN_POINT ( 'NONE',  ( -5.238334947888650284, -36.57199107895616663, -3.000000000000000000 ) ) ;
#5338=EDGE_CURVE ( 'NONE', #736, #7389, #3076, .T. ) ;
#5354=CIRCLE ( 'NONE', #2468, 0.7500000000000041078 ) ;
#5355=PLANE ( 'NONE',  #3688 ) ;
#5358=CYLINDRICAL_SURFACE ( 'NONE', #7234, 37.50000000000000000 ) ;
#5362=CLOSED_SHELL ( 'NONE', ( #1842, #1864, #1250, #2683, #2020, #2786, #2352, #747, #1386, #942, #4313, #3613, #5057, #6685, #2422, #5708, #5684, #7111, #1277, #7598, #1742, #901 ) ) ;
#5373=AXIS2_PLACEMENT_3D ( 'NONE', #7384, #2658, #3321 ) ;
#5374=DIRECTION ( 'NONE',  ( 0.9914448613738101601, -0.1305261922200541547, 0.000000000000000000 ) ) ;
#5378=AXIS2_PLACEMENT_3D ( 'NONE', #3993, #3485, #4545 ) ;
#5380=ORIENTED_EDGE ( 'NONE', *, *, #6197, .F. ) ;
#5432=CIRCLE ( 'NONE', #2039, 6.099504629071904382 ) ;
#5452=ORIENTED_EDGE ( 'NONE', *, *, #4512, .T. ) ;
#5459=CYLINDRICAL_SURFACE ( 'NONE', #1607, 28.49999999999999645 ) ;
#5461=CARTESIAN_POINT ( 'NONE',  ( 4.000000000000000000, -33.63777638310832430, -3.000000000000000000 ) ) ;
#5470=FACE_OUTER_BOUND ( 'NONE', #4079, .T. ) ;
#5495=CARTESIAN_POINT ( 'NONE',  ( -32.81578194438969120, 1.484218055610309728, -3.000000000000000000 ) ) ;
#5496=CARTESIAN_POINT ( 'NONE',  ( -0.7500000000000000000, -37.49249924984995630, 0.000000000000000000 ) ) ;
#5508=LINE ( 'NONE', #4097, #5582 ) ;
#5515=CIRCLE ( 'NONE', #3995, 32.81578194438969120 ) ;
#5540=DIRECTION ( 'NONE',  ( 0.000000000000000000, 0.000000000000000000, 1.000000000000000000 ) ) ;
#5543=CARTESIAN_POINT ( 'NONE',  ( -0.7500000000000000000, -37.49249924984995630, -3.000000000000000000 ) ) ;
#5553=DIRECTION ( 'NONE',  ( 0.000000000000000000, 0.000000000000000000, 1.000000000000000000 ) ) ;
#5555=FILL_AREA_STYLE ('',( #3306 ) ) ;
#5569=FACE_OUTER_BOUND ( 'NONE', #1630, .T. ) ;
#5576=EDGE_CURVE ( 'NONE', #7389, #7629, #1715, .T. ) ;
#5582=VECTOR ( 'NONE', #1924, 1000.000000000000000 ) ;
#5584=EDGE_CURVE ( 'NONE', #3312, #6072, #1307, .T. ) ;
#5587=PRODUCT_CONTEXT ( 'NONE', #1220, 'mechanical' ) ;
#5591=ORIENTED_EDGE ( 'NONE', *, *, #5338, .T. ) ;
#5596=DIRECTION ( 'NONE',  ( 1.000000000000000000, 0.000000000000000000, 0.000000000000000000 ) ) ;
#5601=VECTOR ( 'NONE', #674, 999.9999999999998863 ) ;
#5654=CARTESIAN_POINT ( 'NONE',  ( 0.000000000000000000, 0.000000000000000000, -3.000000000000000000 ) ) ;
#5681=AXIS2_PLACEMENT_3D ( 'NONE', #2014, #5072, #7480 ) ;
#5684=ADVANCED_FACE ( 'NONE', ( #5194 ), #5358, .T. ) ;
#5687=LINE ( 'NONE', #1468, #4383 ) ;
#5708=ADVANCED_FACE ( 'NONE', ( #2373 ), #7170, .T. ) ;
#5714=CARTESIAN_POINT ( 'NONE',  ( -11.50644898236017433, -35.69105814929478981, 0.000000000000000000 ) ) ;
#5723=DIRECTION ( 'NONE',  ( 0.000000000000000000, 0.000000000000000000, 1.000000000000000000 ) ) ;
#5744=CARTESIAN_POINT ( 'NONE',  ( -4.000000000000000000, -33.63777638310832430, -3.000000000000000000 ) ) ;
#5761=EDGE_CURVE ( 'NONE', #3153, #6982, #7364, .T. ) ;
#5767=ORIENTED_EDGE ( 'NONE', *, *, #6977, .F. ) ;
#5777=EDGE_CURVE ( 'NONE', #3595, #1611, #6143, .T. ) ;
#5813=CARTESIAN_POINT ( 'NONE',  ( -28.49999999999999645, 3.490243377569956456E-15, -3.000000000000000000 ) ) ;
#5814=DIRECTION ( 'NONE',  ( 0.000000000000000000, 0.000000000000000000, 1.000000000000000000 ) ) ;
#5815=CARTESIAN_POINT ( 'NONE',  ( 2.750000000000000000, -33.63777638310832430, -3.000000000000000000 ) ) ;
#5850=LINE ( 'NONE', #6444, #7270 ) ;
#5851=DIRECTION ( 'NONE',  ( 1.000000000000000000, 0.000000000000000000, -0.000000000000000000 ) ) ;
#5853=FACE_OUTER_BOUND ( 'NONE', #7421, .T. ) ;
#5856=STYLED_ITEM ( 'NONE', ( #4449 ), #6328 ) ;
#5861=ORIENTED_EDGE ( 'NONE', *, *, #2224, .T. ) ;
#5874=AXIS2_PLACEMENT_3D ( 'NONE', #2666, #6885, #6810 ) ;
#5875=ORIENTED_EDGE ( 'NONE', *, *, #2362, .T. ) ;
#5880=EDGE_CURVE ( 'NONE', #502, #3517, #3815, .T. ) ;
#5887=AXIS2_PLACEMENT_3D ( 'NONE', #7675, #7207, #1810 ) ;
#5895=LINE ( 'NONE', #2363, #5986 ) ;
#5898=CIRCLE ( 'NONE', #974, 37.50000000000000000 ) ;
#5909=CIRCLE ( 'NONE', #2765, 28.49999999999999645 ) ;
#5918=EDGE_CURVE ( 'NONE', #4626, #545, #5354, .T. ) ;
#5920=EDGE_CURVE ( 'NONE', #6434, #421, #5895, .T. ) ;
#5924=DIRECTION ( 'NONE',  ( 0.000000000000000000, 0.000000000000000000, 1.000000000000000000 ) ) ;
#5943=DIRECTION ( 'NONE',  ( 1.000000000000000000, 0.000000000000000000, 0.000000000000000000 ) ) ;
#5952=ORIENTED_EDGE ( 'NONE', *, *, #6226, .F. ) ;
#5956=AXIS2_PLACEMENT_3D ( 'NONE', #6199, #7491, #163 ) ;
#5977=DIRECTION ( 'NONE',  ( 1.000000000000000000, 0.000000000000000000, 0.000000000000000000 ) ) ;
#5984=ORIENTED_EDGE ( 'NONE', *, *, #2061, .F. ) ;
#5986=VECTOR ( 'NONE', #6963, 1000.000000000000000 ) ;
#5991=CARTESIAN_POINT ( 'NONE',  ( -4.586480920263581673, -37.21846574978686562, 0.000000000000000000 ) ) ;
#5992=ORIENTED_EDGE ( 'NONE', *, *, #3212, .T. ) ;
#5996=DIRECTION ( 'NONE',  ( 0.000000000000000000, 0.000000000000000000, 1.000000000000000000 ) ) ;
#6005=CIRCLE ( 'NONE', #3982, 1.250000000000000222 ) ;
#6006=PLANE ( 'NONE',  #1612 ) ;
#6012=ORIENTED_EDGE ( 'NONE', *, *, #1981, .F. ) ;
#6036=ORIENTED_EDGE ( 'NONE', *, *, #3747, .T. ) ;
#6049=VECTOR ( 'NONE', #2054, 1000.000000000000000 ) ;
#6062=EDGE_CURVE ( 'NONE', #2536, #3320, #1064, .T. ) ;
#6072=VERTEX_POINT ( 'NONE', #4273 ) ;
#6105=DIRECTION ( 'NONE',  ( 0.01999999999999999001, -0.9997999799959990108, 0.000000000000000000 ) ) ;
#6108=ORIENTED_EDGE ( 'NONE', *, *, #2175, .F. ) ;
#6114=DIRECTION ( 'NONE',  ( 1.000000000000000000, 0.000000000000000000, 0.000000000000000000 ) ) ;
#6139=AXIS2_PLACEMENT_3D ( 'NONE', #6334, #6961, #1554 ) ;
#6143=LINE ( 'NONE', #2447, #2587 ) ;
#6152=( NAMED_UNIT ( * ) SI_UNIT ( $, .STERADIAN. ) SOLID_ANGLE_UNIT ( ) );
#6160=EDGE_CURVE ( 'NONE', #6072, #3312, #6617, .T. ) ;
#6169=EDGE_CURVE ( 'NONE', #3008, #3001, #1314, .T. ) ;
#6192=( NAMED_UNIT ( * ) PLANE_ANGLE_UNIT ( ) SI_UNIT ( $, .RADIAN. ) );
#6197=EDGE_CURVE ( 'NONE', #4638, #5113, #137, .T. ) ;
#6199=CARTESIAN_POINT ( 'NONE',  ( 0.000000000000000000, 1.484218055610305731, 0.000000000000000000 ) ) ;
#6210=CARTESIAN_POINT ( 'NONE',  ( -2.750000000000000000, -33.63777638310832430, -3.000000000000000000 ) ) ;
#6226=EDGE_CURVE ( 'NONE', #2100, #6929, #2438, .T. ) ;
#6229=CARTESIAN_POINT ( 'NONE',  ( -2.750000000000000000, -33.63777638310832430, -3.000000000000000000 ) ) ;
#6231=SHAPE_REPRESENTATION_RELATIONSHIP ( 'NONE' , 'NONE' ,  #2306, #6328 ) ;
#6236=LINE ( 'NONE', #196, #1783 ) ;
#6247=DIRECTION ( 'NONE',  ( 1.000000000000000000, 0.000000000000000000, 0.000000000000000000 ) ) ;
#6250=CIRCLE ( 'NONE', #1461, 37.50000000000000000 ) ;
#6272=ORIENTED_EDGE ( 'NONE', *, *, #3694, .T. ) ;
#6274=AXIS2_PLACEMENT_3D ( 'NONE', #5815, #5263, #7625 ) ;
#6291=VECTOR ( 'NONE', #2601, 1000.000000000000000 ) ;
#6319=AXIS2_PLACEMENT_3D ( 'NONE', #3194, #2641, #5596 ) ;
#6322=ORIENTED_EDGE ( 'NONE', *, *, #6887, .T. ) ;
#6328=ADVANCED_BREP_SHAPE_REPRESENTATION ( '', ( #475, #7485 ), #6367 ) ;
#6334=CARTESIAN_POINT ( 'NONE',  ( -4.494751301858288528, -36.47409643479112162, 0.000000000000000000 ) ) ;
#6342=DIRECTION ( 'NONE',  ( 1.000000000000000000, 0.000000000000000000, 0.000000000000000000 ) ) ;
#6357=VERTEX_POINT ( 'NONE', #1957 ) ;
#6367=( GEOMETRIC_REPRESENTATION_CONTEXT ( 3 ) GLOBAL_UNCERTAINTY_ASSIGNED_CONTEXT ( ( #7387 ) ) GLOBAL_UNIT_ASSIGNED_CONTEXT ( ( #1979, #4369, #6152 ) ) REPRESENTATION_CONTEXT ( 'NONE', 'WORKASPACE' ) );
#6378=ORIENTED_EDGE ( 'NONE', *, *, #1668, .F. ) ;
#6394=CARTESIAN_POINT ( 'NONE',  ( -9.702951051037022268, -29.86427928513813512, 0.000000000000000000 ) ) ;
#6400=EDGE_CURVE ( 'NONE', #7233, #6357, #6835, .T. ) ;
#6418=ORIENTED_EDGE ( 'NONE', *, *, #6062, .F. ) ;
#6434=VERTEX_POINT ( 'NONE', #7656 ) ;
#6444=CARTESIAN_POINT ( 'NONE',  ( 0.5700000000000001732, -28.49429942988597020, 0.000000000000000000 ) ) ;
#6452=ORIENTED_EDGE ( 'NONE', *, *, #6160, .F. ) ;
#6455=DIRECTION ( 'NONE',  ( -0.000000000000000000, -0.000000000000000000, -1.000000000000000000 ) ) ;
#6462=ORIENTED_EDGE ( 'NONE', *, *, #268, .T. ) ;
#6468=DIRECTION ( 'NONE',  ( 0.000000000000000000, 0.000000000000000000, 1.000000000000000000 ) ) ;
#6486=DIRECTION ( 'NONE',  ( 0.000000000000000000, 0.000000000000000000, 1.000000000000000000 ) ) ;
#6491=ORIENTED_EDGE ( 'NONE', *, *, #4024, .F. ) ;
#6541=DIRECTION ( 'NONE',  ( 1.000000000000000000, 0.000000000000000000, 0.000000000000000000 ) ) ;
#6596=CARTESIAN_POINT ( 'NONE',  ( 32.81578194438969120, 1.484218055610305731, 0.000000000000000000 ) ) ;
#6617=CIRCLE ( 'NONE', #2091, 1.250000000000000444 ) ;
#6624=ORIENTED_EDGE ( 'NONE', *, *, #6169, .T. ) ;
#6638=DIRECTION ( 'NONE',  ( 0.000000000000000000, 0.000000000000000000, 1.000000000000000000 ) ) ;
#6652=AXIS2_PLACEMENT_3D ( 'NONE', #3447, #6486, #4075 ) ;
#6677=ORIENTED_EDGE ( 'NONE', *, *, #2461, .T. ) ;
#6684=UNCERTAINTY_MEASURE_WITH_UNIT (LENGTH_MEASURE( 1.000000000000000082E-05 ), #2818, 'distance_accuracy_value', 'NONE');
#6685=ADVANCED_FACE ( 'NONE', ( #4226 ), #1189, .F. ) ;
#6694=CIRCLE ( 'NONE', #3291, 1.250000000000000444 ) ;
#6702=CARTESIAN_POINT ( 'NONE',  ( -28.49999999999999645, 3.490243377569956456E-15, 0.000000000000000000 ) ) ;
#6708=DIRECTION ( 'NONE',  ( 1.000000000000000000, 0.000000000000000000, 0.000000000000000000 ) ) ;
#6719=CARTESIAN_POINT ( 'NONE',  ( 4.586480920263560357, -37.21846574978686562, 0.000000000000000000 ) ) ;
#6738=EDGE_LOOP ( 'NONE', ( #6108, #7341, #7553, #6933 ) ) ;
#6762=CIRCLE ( 'NONE', #1984, 32.81578194438969120 ) ;
#6770=APPLICATION_CONTEXT ( 'automotive_design' ) ;
#6786=SURFACE_STYLE_USAGE ( .BOTH. , #2016 ) ;
#6793=AXIS2_PLACEMENT_3D ( 'NONE', #4831, #7206, #100 ) ;
#6796=EDGE_CURVE ( 'NONE', #3517, #3380, #4188, .T. ) ;
#6810=DIRECTION ( 'NONE',  ( 1.000000000000000000, 0.000000000000000000, 0.000000000000000000 ) ) ;
#6824=CARTESIAN_POINT ( 'NONE',  ( -4.494751301858288528, -36.47409643479112162, -3.000000000000000000 ) ) ;
#6835=CIRCLE ( 'NONE', #7575, 1.250000000000000444 ) ;
#6850=CYLINDRICAL_SURFACE ( 'NONE', #3749, 1.250000000000000222 ) ;
#6852=CARTESIAN_POINT ( 'NONE',  ( 4.494751301858288528, -36.47409643479112162, -3.000000000000000000 ) ) ;
#6861=( LENGTH_UNIT ( ) NAMED_UNIT ( * ) SI_UNIT ( .MILLI., .METRE. ) );
#6870=VERTEX_POINT ( 'NONE', #6394 ) ;
#6885=DIRECTION ( 'NONE',  ( -0.000000000000000000, -0.000000000000000000, -1.000000000000000000 ) ) ;
#6887=EDGE_CURVE ( 'NONE', #421, #5007, #5249, .T. ) ;
#6910=ORIENTED_EDGE ( 'NONE', *, *, #4964, .F. ) ;
#6926=DIRECTION ( 'NONE',  ( 0.000000000000000000, 0.000000000000000000, 1.000000000000000000 ) ) ;
#6929=VERTEX_POINT ( 'NONE', #1659 ) ;
#6933=ORIENTED_EDGE ( 'NONE', *, *, #6197, .T. ) ;
#6948=CYLINDRICAL_SURFACE ( 'NONE', #7007, 1.250000000000000444 ) ;
#6950=LINE ( 'NONE', #3953, #3379 ) ;
#6954=FACE_OUTER_BOUND ( 'NONE', #1034, .T. ) ;
#6961=DIRECTION ( 'NONE',  ( 0.000000000000000000, 0.000000000000000000, 1.000000000000000000 ) ) ;
#6963=DIRECTION ( 'NONE',  ( 0.01999999999999999001, -0.9997999799959990108, 0.000000000000000000 ) ) ;
#6972=CARTESIAN_POINT ( 'NONE',  ( -32.81578194438969120, 1.484218055610309728, -3.000000000000000000 ) ) ;
#6977=EDGE_CURVE ( 'NONE', #7680, #3299, #3319, .T. ) ;
#6982=VERTEX_POINT ( 'NONE', #3430 ) ;
#7007=AXIS2_PLACEMENT_3D ( 'NONE', #4693, #984, #3477 ) ;
#7008=CARTESIAN_POINT ( 'NONE',  ( 0.000000000000000000, 0.000000000000000000, 0.000000000000000000 ) ) ;
#7019=CIRCLE ( 'NONE', #210, 0.7500000000000041078 ) ;
#7025=VECTOR ( 'NONE', #761, 1000.000000000000000 ) ;
#7038=DIRECTION ( 'NONE',  ( 1.000000000000000000, 0.000000000000000000, 0.000000000000000000 ) ) ;
#7043=ORIENTED_EDGE ( 'NONE', *, *, #268, .F. ) ;
#7053=ORIENTED_EDGE ( 'NONE', *, *, #4512, .F. ) ;
#7062=AXIS2_PLACEMENT_3D ( 'NONE', #3587, #5996, #4214 ) ;
#7065=CIRCLE ( 'NONE', #5681, 28.49999999999999645 ) ;
#7078=DIRECTION ( 'NONE',  ( -1.000000000000000000, 0.000000000000000000, 0.000000000000000000 ) ) ;
#7111=ADVANCED_FACE ( 'NONE', ( #5470 ), #4877, .T. ) ;
#7116=EDGE_CURVE ( 'NONE', #6357, #3312, #5508, .T. ) ;
#7151=ORIENTED_EDGE ( 'NONE', *, *, #3974, .F. ) ;
#7159=DIRECTION ( 'NONE',  ( 0.000000000000000000, 0.000000000000000000, 1.000000000000000000 ) ) ;
#7170=CYLINDRICAL_SURFACE ( 'NONE', #3709, 0.7500000000000041078 ) ;
#7180=VECTOR ( 'NONE', #3188, 1000.000000000000000 ) ;
#7185=EDGE_LOOP ( 'NONE', ( #6910, #278, #6462, #7053 ) ) ;
#7206=DIRECTION ( 'NONE',  ( 0.000000000000000000, 0.000000000000000000, 1.000000000000000000 ) ) ;
#7207=DIRECTION ( 'NONE',  ( 0.000000000000000000, 0.000000000000000000, 1.000000000000000000 ) ) ;
#7211=VECTOR ( 'NONE', #1274, 1000.000000000000000 ) ;
#7233=VERTEX_POINT ( 'NONE', #5744 ) ;
#7234=AXIS2_PLACEMENT_3D ( 'NONE', #3541, #1167, #4010 ) ;
#7240=CARTESIAN_POINT ( 'NONE',  ( -0.5700000000000001732, -28.49429942988597020, 0.000000000000000000 ) ) ;
#7256=DIRECTION ( 'NONE',  ( 1.000000000000000000, 0.000000000000000000, 0.000000000000000000 ) ) ;
#7264=CARTESIAN_POINT ( 'NONE',  ( 9.702951051037011609, -29.86427928513813868, 0.000000000000000000 ) ) ;
#7270=VECTOR ( 'NONE', #1028, 1000.000000000000000 ) ;
#7286=DIRECTION ( 'NONE',  ( 0.1305261922200541547, -0.9914448613738101601, 0.000000000000000000 ) ) ;
#7289=CARTESIAN_POINT ( 'NONE',  ( 0.5700000000000001732, -28.49429942988597020, -3.000000000000000000 ) ) ;
#7299=CIRCLE ( 'NONE', #1499, 32.81578194438969120 ) ;
#7300=ORIENTED_EDGE ( 'NONE', *, *, #7647, .F. ) ;
#7304=CARTESIAN_POINT ( 'NONE',  ( -11.50644898236017433, -35.69105814929478981, -3.000000000000000000 ) ) ;
#7305=CARTESIAN_POINT ( 'NONE',  ( 32.81578194438969120, 1.484218055610305731, -3.000000000000000000 ) ) ;
#7309=PRODUCT_DEFINITION_SHAPE ( 'NONE', 'NONE',  #4161 ) ;
#7341=ORIENTED_EDGE ( 'NONE', *, *, #2224, .F. ) ;
#7364=LINE ( 'NONE', #3109, #2831 ) ;
#7384=CARTESIAN_POINT ( 'NONE',  ( -0.5700000000000001732, -28.49429942988597020, -3.000000000000000000 ) ) ;
#7387=UNCERTAINTY_MEASURE_WITH_UNIT (LENGTH_MEASURE( 1.000000000000000082E-05 ), #1979, 'distance_accuracy_value', 'NONE');
#7389=VERTEX_POINT ( 'NONE', #645 ) ;
#7395=CARTESIAN_POINT ( 'NONE',  ( 4.586480920263560357, -37.21846574978686562, -3.000000000000000000 ) ) ;
#7398=VERTEX_POINT ( 'NONE', #133 ) ;
#7402=ORIENTED_EDGE ( 'NONE', *, *, #7116, .T. ) ;
#7421=EDGE_LOOP ( 'NONE', ( #3491, #825, #781, #2093 ) ) ;
#7471=DIRECTION ( 'NONE',  ( 1.000000000000000000, 0.000000000000000000, 0.000000000000000000 ) ) ;
#7480=DIRECTION ( 'NONE',  ( 1.000000000000000000, 0.000000000000000000, 0.000000000000000000 ) ) ;
#7481=CARTESIAN_POINT ( 'NONE',  ( -4.000000000000000000, -33.63777638310832430, -3.000000000000000000 ) ) ;
#7485=AXIS2_PLACEMENT_3D ( 'NONE', #1301, #3758, #5977 ) ;
#7491=DIRECTION ( 'NONE',  ( 0.000000000000000000, 0.000000000000000000, 1.000000000000000000 ) ) ;
#7506=CARTESIAN_POINT ( 'NONE',  ( 4.494751301858288528, -36.47409643479112162, 0.000000000000000000 ) ) ;
#7511=EDGE_LOOP ( 'NONE', ( #4004, #3991, #824, #7761 ) ) ;
#7541=DIRECTION ( 'NONE',  ( 0.000000000000000000, 0.000000000000000000, 1.000000000000000000 ) ) ;
#7553=ORIENTED_EDGE ( 'NONE', *, *, #3937, .T. ) ;
#7555=DIRECTION ( 'NONE',  ( 0.000000000000000000, 0.000000000000000000, 1.000000000000000000 ) ) ;
#7568=DIRECTION ( 'NONE',  ( 0.000000000000000000, 0.000000000000000000, 1.000000000000000000 ) ) ;
#7575=AXIS2_PLACEMENT_3D ( 'NONE', #6210, #4505, #5096 ) ;
#7576=ORIENTED_EDGE ( 'NONE', *, *, #794, .T. ) ;
#7591=ORIENTED_EDGE ( 'NONE', *, *, #6796, .F. ) ;
#7598=ADVANCED_FACE ( 'NONE', ( #1513, #2859, #918 ), #956, .T. ) ;
#7599=VERTEX_POINT ( 'NONE', #5813 ) ;
#7625=DIRECTION ( 'NONE',  ( 1.000000000000000000, 0.000000000000000000, 0.000000000000000000 ) ) ;
#7629=VERTEX_POINT ( 'NONE', #877 ) ;
#7647=EDGE_CURVE ( 'NONE', #1532, #2100, #2782, .T. ) ;
#7656=CARTESIAN_POINT ( 'NONE',  ( 0.5700000000000001732, -28.49429942988597020, -3.000000000000000000 ) ) ;
#7662=CARTESIAN_POINT ( 'NONE',  ( 5.238334947888644955, -36.57199107895616663, -3.000000000000000000 ) ) ;
#7675=CARTESIAN_POINT ( 'NONE',  ( 0.000000000000000000, 0.000000000000000000, -3.000000000000000000 ) ) ;
#7680=VERTEX_POINT ( 'NONE', #5141 ) ;
#7681=ORIENTED_EDGE ( 'NONE', *, *, #4317, .F. ) ;
#7706=DIRECTION ( 'NONE',  ( 0.000000000000000000, 0.000000000000000000, 1.000000000000000000 ) ) ;
#7713=FACE_OUTER_BOUND ( 'NONE', #1795, .T. ) ;
#7720=EDGE_LOOP ( 'NONE', ( #5147, #2101, #1305, #3781, #5875, #3894, #4983, #4333, #678, #5217, #5452, #6272, #5295, #4673, #4781, #1268 ) ) ;
#7727=ORIENTED_EDGE ( 'NONE', *, *, #610, .F. ) ;
#7758=EDGE_LOOP ( 'NONE', ( #4805, #6452 ) ) ;
#7761=ORIENTED_EDGE ( 'NONE', *, *, #1981, .T. ) ;
#7824=COLOUR_RGB('Grey',0.48,0.52,0.57);
#7825=FILL_AREA_STYLE_COLOUR('',#7824);
#7826=FILL_AREA_STYLE('',(#7825));
#7827=SURFACE_STYLE_FILL_AREA(#7826);
#7828=SURFACE_SIDE_STYLE('',(#7827));
#7829=SURFACE_STYLE_USAGE(.BOTH.,#7828);
#7830=PRESENTATION_STYLE_ASSIGNMENT((#7829));
ENDSEC;
END-ISO-10303-21;
